ISO-10303-21;
HEADER;
/* Generated by software containing ST-Developer
 * from STEP Tools, Inc. (www.steptools.com) 
 */

FILE_DESCRIPTION(
/* description */ ('Double-row support with tensioned shaft'),
/* implementation_level */ '2;1');

FILE_NAME(
/* name */ 'Jam nut.step',
/* time_stamp */ '2026-10-27T10:50:35-07:00',
/* author */ (''),
/* organization */ (''),
/* preprocessor_version */ 'ST-DEVELOPER v20.2',
/* originating_system */ 'Autodesk Translation Framework v15.17.0.0',
/* authorisation */ '');

FILE_SCHEMA (('AUTOMOTIVE_DESIGN { 1 0 10303 214 3 1 1 }'));
ENDSEC;

DATA;
#10=MECHANICAL_DESIGN_GEOMETRIC_PRESENTATION_REPRESENTATION('',(#508),#11559);
#443=SHAPE_REPRESENTATION_RELATIONSHIP('SRR','None',#11753,#475);
#475=ADVANCED_BREP_SHAPE_REPRESENTATION('',(#538),#11555);
#508=STYLED_ITEM('',(#11974),#538);
#538=MANIFOLD_SOLID_BREP('Body1',#6356);
#662=FACE_BOUND('',#1684,.T.);
#663=FACE_BOUND('',#1686,.T.);
#881=PLANE('',#7287);
#882=PLANE('',#7288);
#883=PLANE('',#7289);
#884=PLANE('',#7290);
#885=PLANE('',#7291);
#886=PLANE('',#7292);
#887=PLANE('',#7293);
#888=PLANE('',#7294);
#1212=FACE_OUTER_BOUND('',#1676,.T.);
#1213=FACE_OUTER_BOUND('',#1677,.T.);
#1214=FACE_OUTER_BOUND('',#1678,.T.);
#1215=FACE_OUTER_BOUND('',#1679,.T.);
#1216=FACE_OUTER_BOUND('',#1680,.T.);
#1217=FACE_OUTER_BOUND('',#1681,.T.);
#1218=FACE_OUTER_BOUND('',#1682,.T.);
#1219=FACE_OUTER_BOUND('',#1683,.T.);
#1220=FACE_OUTER_BOUND('',#1685,.T.);
#1676=EDGE_LOOP('',(#5664,#5665,#5666,#5667));
#1677=EDGE_LOOP('',(#5668,#5669,#5670,#5671));
#1678=EDGE_LOOP('',(#5672,#5673,#5674,#5675));
#1679=EDGE_LOOP('',(#5676,#5677,#5678,#5679));
#1680=EDGE_LOOP('',(#5680,#5681,#5682,#5683));
#1681=EDGE_LOOP('',(#5684,#5685,#5686,#5687));
#1682=EDGE_LOOP('',(#5688,#5689,#5690,#5691));
#1683=EDGE_LOOP('',(#5692,#5693,#5694,#5695,#5696,#5697));
#1684=EDGE_LOOP('',(#5698));
#1685=EDGE_LOOP('',(#5699,#5700,#5701,#5702,#5703,#5704));
#1686=EDGE_LOOP('',(#5705));
#2205=LINE('',#11188,#2752);
#2206=LINE('',#11193,#2753);
#2207=LINE('',#11195,#2754);
#2208=LINE('',#11197,#2755);
#2209=LINE('',#11198,#2756);
#2210=LINE('',#11201,#2757);
#2211=LINE('',#11203,#2758);
#2212=LINE('',#11204,#2759);
#2213=LINE('',#11207,#2760);
#2214=LINE('',#11209,#2761);
#2215=LINE('',#11210,#2762);
#2216=LINE('',#11213,#2763);
#2217=LINE('',#11215,#2764);
#2218=LINE('',#11216,#2765);
#2219=LINE('',#11219,#2766);
#2220=LINE('',#11221,#2767);
#2221=LINE('',#11222,#2768);
#2222=LINE('',#11224,#2769);
#2223=LINE('',#11225,#2770);
#2752=VECTOR('',#8980,0.54);
#2753=VECTOR('',#8985,1.);
#2754=VECTOR('',#8986,1.);
#2755=VECTOR('',#8987,1.);
#2756=VECTOR('',#8988,1.);
#2757=VECTOR('',#8991,1.);
#2758=VECTOR('',#8992,1.);
#2759=VECTOR('',#8993,1.);
#2760=VECTOR('',#8996,1.);
#2761=VECTOR('',#8997,1.);
#2762=VECTOR('',#8998,1.);
#2763=VECTOR('',#9001,1.);
#2764=VECTOR('',#9002,1.);
#2765=VECTOR('',#9003,1.);
#2766=VECTOR('',#9006,1.);
#2767=VECTOR('',#9007,1.);
#2768=VECTOR('',#9008,1.);
#2769=VECTOR('',#9011,1.);
#2770=VECTOR('',#9012,1.);
#3002=CIRCLE('',#7285,0.54);
#3003=CIRCLE('',#7286,0.54);
#3475=VERTEX_POINT('',#11185);
#3476=VERTEX_POINT('',#11187);
#3477=VERTEX_POINT('',#11191);
#3478=VERTEX_POINT('',#11192);
#3479=VERTEX_POINT('',#11194);
#3480=VERTEX_POINT('',#11196);
#3481=VERTEX_POINT('',#11200);
#3482=VERTEX_POINT('',#11202);
#3483=VERTEX_POINT('',#11206);
#3484=VERTEX_POINT('',#11208);
#3485=VERTEX_POINT('',#11212);
#3486=VERTEX_POINT('',#11214);
#3487=VERTEX_POINT('',#11218);
#3488=VERTEX_POINT('',#11220);
#4217=EDGE_CURVE('',#3475,#3475,#3002,.T.);
#4218=EDGE_CURVE('',#3475,#3476,#2205,.T.);
#4219=EDGE_CURVE('',#3476,#3476,#3003,.T.);
#4220=EDGE_CURVE('',#3477,#3478,#2206,.T.);
#4221=EDGE_CURVE('',#3477,#3479,#2207,.T.);
#4222=EDGE_CURVE('',#3480,#3479,#2208,.T.);
#4223=EDGE_CURVE('',#3478,#3480,#2209,.T.);
#4224=EDGE_CURVE('',#3478,#3481,#2210,.T.);
#4225=EDGE_CURVE('',#3482,#3480,#2211,.T.);
#4226=EDGE_CURVE('',#3481,#3482,#2212,.T.);
#4227=EDGE_CURVE('',#3481,#3483,#2213,.T.);
#4228=EDGE_CURVE('',#3484,#3482,#2214,.T.);
#4229=EDGE_CURVE('',#3483,#3484,#2215,.T.);
#4230=EDGE_CURVE('',#3483,#3485,#2216,.T.);
#4231=EDGE_CURVE('',#3486,#3484,#2217,.T.);
#4232=EDGE_CURVE('',#3485,#3486,#2218,.T.);
#4233=EDGE_CURVE('',#3485,#3487,#2219,.T.);
#4234=EDGE_CURVE('',#3488,#3486,#2220,.T.);
#4235=EDGE_CURVE('',#3487,#3488,#2221,.T.);
#4236=EDGE_CURVE('',#3487,#3477,#2222,.T.);
#4237=EDGE_CURVE('',#3479,#3488,#2223,.T.);
#5664=ORIENTED_EDGE('',*,*,#4217,.F.);
#5665=ORIENTED_EDGE('',*,*,#4218,.T.);
#5666=ORIENTED_EDGE('',*,*,#4219,.F.);
#5667=ORIENTED_EDGE('',*,*,#4218,.F.);
#5668=ORIENTED_EDGE('',*,*,#4220,.F.);
#5669=ORIENTED_EDGE('',*,*,#4221,.T.);
#5670=ORIENTED_EDGE('',*,*,#4222,.F.);
#5671=ORIENTED_EDGE('',*,*,#4223,.F.);
#5672=ORIENTED_EDGE('',*,*,#4224,.F.);
#5673=ORIENTED_EDGE('',*,*,#4223,.T.);
#5674=ORIENTED_EDGE('',*,*,#4225,.F.);
#5675=ORIENTED_EDGE('',*,*,#4226,.F.);
#5676=ORIENTED_EDGE('',*,*,#4227,.F.);
#5677=ORIENTED_EDGE('',*,*,#4226,.T.);
#5678=ORIENTED_EDGE('',*,*,#4228,.F.);
#5679=ORIENTED_EDGE('',*,*,#4229,.F.);
#5680=ORIENTED_EDGE('',*,*,#4230,.F.);
#5681=ORIENTED_EDGE('',*,*,#4229,.T.);
#5682=ORIENTED_EDGE('',*,*,#4231,.F.);
#5683=ORIENTED_EDGE('',*,*,#4232,.F.);
#5684=ORIENTED_EDGE('',*,*,#4233,.F.);
#5685=ORIENTED_EDGE('',*,*,#4232,.T.);
#5686=ORIENTED_EDGE('',*,*,#4234,.F.);
#5687=ORIENTED_EDGE('',*,*,#4235,.F.);
#5688=ORIENTED_EDGE('',*,*,#4236,.F.);
#5689=ORIENTED_EDGE('',*,*,#4235,.T.);
#5690=ORIENTED_EDGE('',*,*,#4237,.F.);
#5691=ORIENTED_EDGE('',*,*,#4221,.F.);
#5692=ORIENTED_EDGE('',*,*,#4237,.T.);
#5693=ORIENTED_EDGE('',*,*,#4234,.T.);
#5694=ORIENTED_EDGE('',*,*,#4231,.T.);
#5695=ORIENTED_EDGE('',*,*,#4228,.T.);
#5696=ORIENTED_EDGE('',*,*,#4225,.T.);
#5697=ORIENTED_EDGE('',*,*,#4222,.T.);
#5698=ORIENTED_EDGE('',*,*,#4219,.T.);
#5699=ORIENTED_EDGE('',*,*,#4236,.T.);
#5700=ORIENTED_EDGE('',*,*,#4220,.T.);
#5701=ORIENTED_EDGE('',*,*,#4224,.T.);
#5702=ORIENTED_EDGE('',*,*,#4227,.T.);
#5703=ORIENTED_EDGE('',*,*,#4230,.T.);
#5704=ORIENTED_EDGE('',*,*,#4233,.T.);
#5705=ORIENTED_EDGE('',*,*,#4217,.T.);
#5969=CYLINDRICAL_SURFACE('',#7284,0.54);
#6275=ADVANCED_FACE('',(#1212),#5969,.F.);
#6276=ADVANCED_FACE('',(#1213),#881,.T.);
#6277=ADVANCED_FACE('',(#1214),#882,.T.);
#6278=ADVANCED_FACE('',(#1215),#883,.T.);
#6279=ADVANCED_FACE('',(#1216),#884,.T.);
#6280=ADVANCED_FACE('',(#1217),#885,.T.);
#6281=ADVANCED_FACE('',(#1218),#886,.T.);
#6282=ADVANCED_FACE('',(#1219,#662),#887,.T.);
#6283=ADVANCED_FACE('',(#1220,#663),#888,.F.);
#6356=CLOSED_SHELL('',(#6275,#6276,#6277,#6278,#6279,#6280,#6281,#6282,
#6283));
#7283=AXIS2_PLACEMENT_3D('',#11183,#8974,#8975);
#7284=AXIS2_PLACEMENT_3D('',#11184,#8976,#8977);
#7285=AXIS2_PLACEMENT_3D('',#11186,#8978,#8979);
#7286=AXIS2_PLACEMENT_3D('',#11189,#8981,#8982);
#7287=AXIS2_PLACEMENT_3D('',#11190,#8983,#8984);
#7288=AXIS2_PLACEMENT_3D('',#11199,#8989,#8990);
#7289=AXIS2_PLACEMENT_3D('',#11205,#8994,#8995);
#7290=AXIS2_PLACEMENT_3D('',#11211,#8999,#9000);
#7291=AXIS2_PLACEMENT_3D('',#11217,#9004,#9005);
#7292=AXIS2_PLACEMENT_3D('',#11223,#9009,#9010);
#7293=AXIS2_PLACEMENT_3D('',#11226,#9013,#9014);
#7294=AXIS2_PLACEMENT_3D('',#11227,#9015,#9016);
#8974=DIRECTION('axis',(0.,0.,1.));
#8975=DIRECTION('refdir',(1.,0.,0.));
#8976=DIRECTION('center_axis',(0.,1.,0.));
#8977=DIRECTION('ref_axis',(1.,0.,0.));
#8978=DIRECTION('center_axis',(0.,1.,0.));
#8979=DIRECTION('ref_axis',(1.,0.,0.));
#8980=DIRECTION('',(0.,1.,0.));
#8981=DIRECTION('center_axis',(0.,-1.,0.));
#8982=DIRECTION('ref_axis',(1.,0.,0.));
#8983=DIRECTION('center_axis',(0.866025403784439,0.,-0.5));
#8984=DIRECTION('ref_axis',(-0.5,0.,-0.866025403784439));
#8985=DIRECTION('',(0.5,0.,0.866025403784438));
#8986=DIRECTION('',(0.,1.,0.));
#8987=DIRECTION('',(-0.5,0.,-0.866025403784438));
#8988=DIRECTION('',(0.,1.,0.));
#8989=DIRECTION('center_axis',(0.866025403784439,0.,0.5));
#8990=DIRECTION('ref_axis',(0.5,0.,-0.866025403784439));
#8991=DIRECTION('',(-0.5,0.,0.866025403784438));
#8992=DIRECTION('',(0.5,0.,-0.866025403784438));
#8993=DIRECTION('',(0.,1.,0.));
#8994=DIRECTION('center_axis',(0.,0.,1.));
#8995=DIRECTION('ref_axis',(1.,0.,0.));
#8996=DIRECTION('',(-1.,0.,0.));
#8997=DIRECTION('',(1.,0.,0.));
#8998=DIRECTION('',(0.,1.,0.));
#8999=DIRECTION('center_axis',(-0.866025403784438,0.,0.5));
#9000=DIRECTION('ref_axis',(0.5,0.,0.866025403784438));
#9001=DIRECTION('',(-0.5,0.,-0.866025403784438));
#9002=DIRECTION('',(0.5,0.,0.866025403784438));
#9003=DIRECTION('',(0.,1.,0.));
#9004=DIRECTION('center_axis',(-0.866025403784439,0.,-0.5));
#9005=DIRECTION('ref_axis',(-0.5,0.,0.866025403784439));
#9006=DIRECTION('',(0.5,0.,-0.866025403784439));
#9007=DIRECTION('',(-0.5,0.,0.866025403784439));
#9008=DIRECTION('',(0.,1.,0.));
#9009=DIRECTION('center_axis',(0.,0.,-1.));
#9010=DIRECTION('ref_axis',(-1.,0.,0.));
#9011=DIRECTION('',(1.,0.,0.));
#9012=DIRECTION('',(-1.,0.,0.));
#9013=DIRECTION('center_axis',(0.,1.,0.));
#9014=DIRECTION('ref_axis',(0.,0.,1.));
#9015=DIRECTION('center_axis',(0.,1.,0.));
#9016=DIRECTION('ref_axis',(1.,0.,0.));
#11183=CARTESIAN_POINT('',(0.,0.,0.));
#11184=CARTESIAN_POINT('Origin',(0.,21.7,10.));
#11185=CARTESIAN_POINT('',(-0.54,21.8,10.));
#11186=CARTESIAN_POINT('Origin',(0.,21.8,10.));
#11187=CARTESIAN_POINT('',(-0.54,22.6,10.));
#11188=CARTESIAN_POINT('',(-0.54,21.7,10.));
#11189=CARTESIAN_POINT('Origin',(0.,22.6,10.));
#11190=CARTESIAN_POINT('Origin',(1.09696551146029,21.8,10.));
#11191=CARTESIAN_POINT('',(0.548482755730145,21.8,9.05));
#11192=CARTESIAN_POINT('',(1.09696551146029,21.8,10.));
#11193=CARTESIAN_POINT('',(0.548482755730145,21.8,9.05));
#11194=CARTESIAN_POINT('',(0.548482755730145,22.6,9.05));
#11195=CARTESIAN_POINT('',(0.548482755730145,21.8,9.05));
#11196=CARTESIAN_POINT('',(1.09696551146029,22.6,10.));
#11197=CARTESIAN_POINT('',(0.548482755730145,22.6,9.05));
#11198=CARTESIAN_POINT('',(1.09696551146029,21.8,10.));
#11199=CARTESIAN_POINT('Origin',(0.548482755730145,21.8,10.95));
#11200=CARTESIAN_POINT('',(0.548482755730145,21.8,10.95));
#11201=CARTESIAN_POINT('',(1.09696551146029,21.8,10.));
#11202=CARTESIAN_POINT('',(0.548482755730145,22.6,10.95));
#11203=CARTESIAN_POINT('',(1.09696551146029,22.6,10.));
#11204=CARTESIAN_POINT('',(0.548482755730145,21.8,10.95));
#11205=CARTESIAN_POINT('Origin',(-0.548482755730144,21.8,10.95));
#11206=CARTESIAN_POINT('',(-0.548482755730144,21.8,10.95));
#11207=CARTESIAN_POINT('',(0.548482755730145,21.8,10.95));
#11208=CARTESIAN_POINT('',(-0.548482755730144,22.6,10.95));
#11209=CARTESIAN_POINT('',(0.548482755730145,22.6,10.95));
#11210=CARTESIAN_POINT('',(-0.548482755730144,21.8,10.95));
#11211=CARTESIAN_POINT('Origin',(-1.09696551146029,21.8,10.));
#11212=CARTESIAN_POINT('',(-1.09696551146029,21.8,10.));
#11213=CARTESIAN_POINT('',(-0.548482755730144,21.8,10.95));
#11214=CARTESIAN_POINT('',(-1.09696551146029,22.6,10.));
#11215=CARTESIAN_POINT('',(-0.548482755730144,22.6,10.95));
#11216=CARTESIAN_POINT('',(-1.09696551146029,21.8,10.));
#11217=CARTESIAN_POINT('Origin',(-0.548482755730145,21.8,9.05));
#11218=CARTESIAN_POINT('',(-0.548482755730145,21.8,9.05));
#11219=CARTESIAN_POINT('',(-1.09696551146029,21.8,10.));
#11220=CARTESIAN_POINT('',(-0.548482755730145,22.6,9.05));
#11221=CARTESIAN_POINT('',(-1.09696551146029,22.6,10.));
#11222=CARTESIAN_POINT('',(-0.548482755730145,21.8,9.05));
#11223=CARTESIAN_POINT('Origin',(0.548482755730145,21.8,9.05));
#11224=CARTESIAN_POINT('',(-0.548482755730145,21.8,9.05));
#11225=CARTESIAN_POINT('',(-0.548482755730145,22.6,9.05));
#11226=CARTESIAN_POINT('Origin',(0.,22.6,10.));
#11227=CARTESIAN_POINT('Origin',(0.,21.8,10.));
#11518=UNCERTAINTY_MEASURE_WITH_UNIT(LENGTH_MEASURE(0.001),#11560,
'DISTANCE_ACCURACY_VALUE',
'Maximum model space distance between geometric entities at asserted c
onnectivities');
#11522=UNCERTAINTY_MEASURE_WITH_UNIT(LENGTH_MEASURE(0.001),#11560,
'DISTANCE_ACCURACY_VALUE',
'Maximum model space distance between geometric entities at asserted c
onnectivities');
#11555=(
GEOMETRIC_REPRESENTATION_CONTEXT(3)
GLOBAL_UNCERTAINTY_ASSIGNED_CONTEXT((#11518))
GLOBAL_UNIT_ASSIGNED_CONTEXT((#11560,#11562,#11563))
REPRESENTATION_CONTEXT('','3D')
);
#11559=(
GEOMETRIC_REPRESENTATION_CONTEXT(3)
GLOBAL_UNCERTAINTY_ASSIGNED_CONTEXT((#11522))
GLOBAL_UNIT_ASSIGNED_CONTEXT((#11560,#11562,#11563))
REPRESENTATION_CONTEXT('','3D')
);
#11560=(
LENGTH_UNIT()
NAMED_UNIT(*)
SI_UNIT(.CENTI.,.METRE.)
);
#11562=(
NAMED_UNIT(*)
PLANE_ANGLE_UNIT()
SI_UNIT($,.RADIAN.)
);
#11563=(
NAMED_UNIT(*)
SI_UNIT($,.STERADIAN.)
SOLID_ANGLE_UNIT()
);
#11596=SHAPE_DEFINITION_REPRESENTATION(#11707,#11753);
#11707=PRODUCT_DEFINITION_SHAPE('',$,#11790);
#11753=SHAPE_REPRESENTATION('',(#7283),#11555);
#11757=PRODUCT_DEFINITION_CONTEXT('part definition',#11867,'design');
#11790=PRODUCT_DEFINITION('Jam nut','Jam nut',#11826,#11757);
#11826=PRODUCT_DEFINITION_FORMATION('',$,#11901);
#11867=APPLICATION_CONTEXT(
'Core Data for Automotive Mechanical Design Process');
#11868=PRODUCT_CONTEXT('part definition',#11867,'mechanical');
#11901=PRODUCT('Jam nut','Jam nut','Jam nut',(#11868));
#11968=COLOUR_RGB('Black',0.12,0.14,0.17);
#11969=FILL_AREA_STYLE_COLOUR('',#11968);
#11970=FILL_AREA_STYLE('',(#11969));
#11971=SURFACE_STYLE_FILL_AREA(#11970);
#11972=SURFACE_SIDE_STYLE('',(#11971));
#11973=SURFACE_STYLE_USAGE(.BOTH.,#11972);
#11974=PRESENTATION_STYLE_ASSIGNMENT((#11973));
ENDSEC;
END-ISO-10303-21;
